ISO-10303-21;
HEADER;
/* Generated by software containing ST-Developer
 * from STEP Tools, Inc. (www.steptools.com) 
 */

FILE_DESCRIPTION(
/* description */ ('Torque wrench calibration arm'),
/* implementation_level */ '2;1');

FILE_NAME(
/* name */ 'Socket Set Screw - M5x8.step',
/* time_stamp */ '2026-10-28T03:24:52-07:00',
/* author */ (''),
/* organization */ (''),
/* preprocessor_version */ 'ST-DEVELOPER v20.2',
/* originating_system */ 'Autodesk Translation Framework v15.17.0.0',
/* authorisation */ '');

FILE_SCHEMA (('AUTOMOTIVE_DESIGN { 1 0 10303 214 3 1 1 }'));
ENDSEC;

DATA;
#10=MECHANICAL_DESIGN_GEOMETRIC_PRESENTATION_REPRESENTATION('',(#457),#12783);
#339=CONICAL_SURFACE('',#7530,0.235,0.785398163397448);
#340=CONICAL_SURFACE('',#7534,0.2125,0.785398163397448);
#374=SHAPE_REPRESENTATION_RELATIONSHIP('SRR','None',#12957,#411);
#411=ADVANCED_BREP_SHAPE_REPRESENTATION('',(#509),#12766);
#457=STYLED_ITEM('',(#13219),#509);
#509=MANIFOLD_SOLID_BREP('Body1',#6528);
#621=FACE_BOUND('',#1640,.T.);
#812=PLANE('',#7521);
#813=PLANE('',#7522);
#814=PLANE('',#7523);
#815=PLANE('',#7524);
#816=PLANE('',#7525);
#817=PLANE('',#7526);
#818=PLANE('',#7527);
#819=PLANE('',#7528);
#820=PLANE('',#7536);
#1147=FACE_OUTER_BOUND('',#1632,.T.);
#1148=FACE_OUTER_BOUND('',#1633,.T.);
#1149=FACE_OUTER_BOUND('',#1634,.T.);
#1150=FACE_OUTER_BOUND('',#1635,.T.);
#1151=FACE_OUTER_BOUND('',#1636,.T.);
#1152=FACE_OUTER_BOUND('',#1637,.T.);
#1153=FACE_OUTER_BOUND('',#1638,.T.);
#1154=FACE_OUTER_BOUND('',#1639,.T.);
#1155=FACE_OUTER_BOUND('',#1641,.T.);
#1156=FACE_OUTER_BOUND('',#1642,.T.);
#1157=FACE_OUTER_BOUND('',#1643,.T.);
#1158=FACE_OUTER_BOUND('',#1644,.T.);
#1632=EDGE_LOOP('',(#5509,#5510,#5511,#5512));
#1633=EDGE_LOOP('',(#5513,#5514,#5515,#5516));
#1634=EDGE_LOOP('',(#5517,#5518,#5519,#5520));
#1635=EDGE_LOOP('',(#5521,#5522,#5523,#5524));
#1636=EDGE_LOOP('',(#5525,#5526,#5527,#5528));
#1637=EDGE_LOOP('',(#5529,#5530,#5531,#5532));
#1638=EDGE_LOOP('',(#5533,#5534,#5535,#5536,#5537,#5538));
#1639=EDGE_LOOP('',(#5539));
#1640=EDGE_LOOP('',(#5540,#5541,#5542,#5543,#5544,#5545));
#1641=EDGE_LOOP('',(#5546,#5547,#5548,#5549));
#1642=EDGE_LOOP('',(#5550,#5551,#5552,#5553));
#1643=EDGE_LOOP('',(#5554,#5555,#5556,#5557));
#1644=EDGE_LOOP('',(#5558));
#2099=LINE('',#11785,#2514);
#2100=LINE('',#11787,#2515);
#2101=LINE('',#11789,#2516);
#2102=LINE('',#11790,#2517);
#2103=LINE('',#11793,#2518);
#2104=LINE('',#11795,#2519);
#2105=LINE('',#11796,#2520);
#2106=LINE('',#11799,#2521);
#2107=LINE('',#11801,#2522);
#2108=LINE('',#11802,#2523);
#2109=LINE('',#11805,#2524);
#2110=LINE('',#11807,#2525);
#2111=LINE('',#11808,#2526);
#2112=LINE('',#11811,#2527);
#2113=LINE('',#11813,#2528);
#2114=LINE('',#11814,#2529);
#2115=LINE('',#11816,#2530);
#2116=LINE('',#11817,#2531);
#2117=LINE('',#11825,#2532);
#2118=LINE('',#11829,#2533);
#2119=LINE('',#11833,#2534);
#2514=VECTOR('',#9247,1.);
#2515=VECTOR('',#9248,1.);
#2516=VECTOR('',#9249,1.);
#2517=VECTOR('',#9250,1.);
#2518=VECTOR('',#9253,1.);
#2519=VECTOR('',#9254,1.);
#2520=VECTOR('',#9255,1.);
#2521=VECTOR('',#9258,1.);
#2522=VECTOR('',#9259,1.);
#2523=VECTOR('',#9260,1.);
#2524=VECTOR('',#9263,1.);
#2525=VECTOR('',#9264,1.);
#2526=VECTOR('',#9265,1.);
#2527=VECTOR('',#9268,1.);
#2528=VECTOR('',#9269,1.);
#2529=VECTOR('',#9270,1.);
#2530=VECTOR('',#9273,1.);
#2531=VECTOR('',#9274,1.);
#2532=VECTOR('',#9285,0.235);
#2533=VECTOR('',#9290,0.25);
#2534=VECTOR('',#9295,0.2125);
#2852=CIRCLE('',#7529,0.22);
#2853=CIRCLE('',#7531,0.24505);
#2854=CIRCLE('',#7533,0.24505);
#2855=CIRCLE('',#7535,0.175);
#3366=VERTEX_POINT('',#11783);
#3367=VERTEX_POINT('',#11784);
#3368=VERTEX_POINT('',#11786);
#3369=VERTEX_POINT('',#11788);
#3370=VERTEX_POINT('',#11792);
#3371=VERTEX_POINT('',#11794);
#3372=VERTEX_POINT('',#11798);
#3373=VERTEX_POINT('',#11800);
#3374=VERTEX_POINT('',#11804);
#3375=VERTEX_POINT('',#11806);
#3376=VERTEX_POINT('',#11810);
#3377=VERTEX_POINT('',#11812);
#3378=VERTEX_POINT('',#11820);
#3379=VERTEX_POINT('',#11823);
#3380=VERTEX_POINT('',#11827);
#3381=VERTEX_POINT('',#11831);
#4112=EDGE_CURVE('',#3366,#3367,#2099,.T.);
#4113=EDGE_CURVE('',#3366,#3368,#2100,.T.);
#4114=EDGE_CURVE('',#3368,#3369,#2101,.T.);
#4115=EDGE_CURVE('',#3367,#3369,#2102,.T.);
#4116=EDGE_CURVE('',#3370,#3366,#2103,.T.);
#4117=EDGE_CURVE('',#3370,#3371,#2104,.T.);
#4118=EDGE_CURVE('',#3371,#3368,#2105,.T.);
#4119=EDGE_CURVE('',#3372,#3370,#2106,.T.);
#4120=EDGE_CURVE('',#3372,#3373,#2107,.T.);
#4121=EDGE_CURVE('',#3373,#3371,#2108,.T.);
#4122=EDGE_CURVE('',#3374,#3372,#2109,.T.);
#4123=EDGE_CURVE('',#3374,#3375,#2110,.T.);
#4124=EDGE_CURVE('',#3375,#3373,#2111,.T.);
#4125=EDGE_CURVE('',#3376,#3374,#2112,.T.);
#4126=EDGE_CURVE('',#3376,#3377,#2113,.T.);
#4127=EDGE_CURVE('',#3377,#3375,#2114,.T.);
#4128=EDGE_CURVE('',#3367,#3376,#2115,.T.);
#4129=EDGE_CURVE('',#3369,#3377,#2116,.T.);
#4130=EDGE_CURVE('',#3378,#3378,#2852,.T.);
#4131=EDGE_CURVE('',#3379,#3379,#2853,.T.);
#4132=EDGE_CURVE('',#3379,#3378,#2117,.T.);
#4133=EDGE_CURVE('',#3380,#3380,#2854,.F.);
#4134=EDGE_CURVE('',#3380,#3379,#2118,.T.);
#4135=EDGE_CURVE('',#3381,#3381,#2855,.T.);
#4136=EDGE_CURVE('',#3381,#3380,#2119,.T.);
#5509=ORIENTED_EDGE('',*,*,#4112,.F.);
#5510=ORIENTED_EDGE('',*,*,#4113,.T.);
#5511=ORIENTED_EDGE('',*,*,#4114,.T.);
#5512=ORIENTED_EDGE('',*,*,#4115,.F.);
#5513=ORIENTED_EDGE('',*,*,#4116,.F.);
#5514=ORIENTED_EDGE('',*,*,#4117,.T.);
#5515=ORIENTED_EDGE('',*,*,#4118,.T.);
#5516=ORIENTED_EDGE('',*,*,#4113,.F.);
#5517=ORIENTED_EDGE('',*,*,#4119,.F.);
#5518=ORIENTED_EDGE('',*,*,#4120,.T.);
#5519=ORIENTED_EDGE('',*,*,#4121,.T.);
#5520=ORIENTED_EDGE('',*,*,#4117,.F.);
#5521=ORIENTED_EDGE('',*,*,#4122,.F.);
#5522=ORIENTED_EDGE('',*,*,#4123,.T.);
#5523=ORIENTED_EDGE('',*,*,#4124,.T.);
#5524=ORIENTED_EDGE('',*,*,#4120,.F.);
#5525=ORIENTED_EDGE('',*,*,#4125,.F.);
#5526=ORIENTED_EDGE('',*,*,#4126,.T.);
#5527=ORIENTED_EDGE('',*,*,#4127,.T.);
#5528=ORIENTED_EDGE('',*,*,#4123,.F.);
#5529=ORIENTED_EDGE('',*,*,#4128,.F.);
#5530=ORIENTED_EDGE('',*,*,#4115,.T.);
#5531=ORIENTED_EDGE('',*,*,#4129,.T.);
#5532=ORIENTED_EDGE('',*,*,#4126,.F.);
#5533=ORIENTED_EDGE('',*,*,#4129,.F.);
#5534=ORIENTED_EDGE('',*,*,#4114,.F.);
#5535=ORIENTED_EDGE('',*,*,#4118,.F.);
#5536=ORIENTED_EDGE('',*,*,#4121,.F.);
#5537=ORIENTED_EDGE('',*,*,#4124,.F.);
#5538=ORIENTED_EDGE('',*,*,#4127,.F.);
#5539=ORIENTED_EDGE('',*,*,#4130,.F.);
#5540=ORIENTED_EDGE('',*,*,#4112,.T.);
#5541=ORIENTED_EDGE('',*,*,#4128,.T.);
#5542=ORIENTED_EDGE('',*,*,#4125,.T.);
#5543=ORIENTED_EDGE('',*,*,#4122,.T.);
#5544=ORIENTED_EDGE('',*,*,#4119,.T.);
#5545=ORIENTED_EDGE('',*,*,#4116,.T.);
#5546=ORIENTED_EDGE('',*,*,#4131,.F.);
#5547=ORIENTED_EDGE('',*,*,#4132,.T.);
#5548=ORIENTED_EDGE('',*,*,#4130,.T.);
#5549=ORIENTED_EDGE('',*,*,#4132,.F.);
#5550=ORIENTED_EDGE('',*,*,#4133,.F.);
#5551=ORIENTED_EDGE('',*,*,#4134,.T.);
#5552=ORIENTED_EDGE('',*,*,#4131,.T.);
#5553=ORIENTED_EDGE('',*,*,#4134,.F.);
#5554=ORIENTED_EDGE('',*,*,#4135,.F.);
#5555=ORIENTED_EDGE('',*,*,#4136,.T.);
#5556=ORIENTED_EDGE('',*,*,#4133,.T.);
#5557=ORIENTED_EDGE('',*,*,#4136,.F.);
#5558=ORIENTED_EDGE('',*,*,#4135,.T.);
#6067=CYLINDRICAL_SURFACE('',#7532,0.24505);
#6372=ADVANCED_FACE('',(#1147),#812,.F.);
#6373=ADVANCED_FACE('',(#1148),#813,.F.);
#6374=ADVANCED_FACE('',(#1149),#814,.F.);
#6375=ADVANCED_FACE('',(#1150),#815,.F.);
#6376=ADVANCED_FACE('',(#1151),#816,.F.);
#6377=ADVANCED_FACE('',(#1152),#817,.F.);
#6378=ADVANCED_FACE('',(#1153),#818,.F.);
#6379=ADVANCED_FACE('',(#1154,#621),#819,.T.);
#6380=ADVANCED_FACE('',(#1155),#339,.T.);
#6381=ADVANCED_FACE('',(#1156),#6067,.T.);
#6382=ADVANCED_FACE('',(#1157),#340,.T.);
#6383=ADVANCED_FACE('',(#1158),#820,.T.);
#6528=CLOSED_SHELL('',(#6372,#6373,#6374,#6375,#6376,#6377,#6378,#6379,
#6380,#6381,#6382,#6383));
#7520=AXIS2_PLACEMENT_3D('',#11781,#9243,#9244);
#7521=AXIS2_PLACEMENT_3D('',#11782,#9245,#9246);
#7522=AXIS2_PLACEMENT_3D('',#11791,#9251,#9252);
#7523=AXIS2_PLACEMENT_3D('',#11797,#9256,#9257);
#7524=AXIS2_PLACEMENT_3D('',#11803,#9261,#9262);
#7525=AXIS2_PLACEMENT_3D('',#11809,#9266,#9267);
#7526=AXIS2_PLACEMENT_3D('',#11815,#9271,#9272);
#7527=AXIS2_PLACEMENT_3D('',#11818,#9275,#9276);
#7528=AXIS2_PLACEMENT_3D('',#11819,#9277,#9278);
#7529=AXIS2_PLACEMENT_3D('',#11821,#9279,#9280);
#7530=AXIS2_PLACEMENT_3D('',#11822,#9281,#9282);
#7531=AXIS2_PLACEMENT_3D('',#11824,#9283,#9284);
#7532=AXIS2_PLACEMENT_3D('',#11826,#9286,#9287);
#7533=AXIS2_PLACEMENT_3D('',#11828,#9288,#9289);
#7534=AXIS2_PLACEMENT_3D('',#11830,#9291,#9292);
#7535=AXIS2_PLACEMENT_3D('',#11832,#9293,#9294);
#7536=AXIS2_PLACEMENT_3D('',#11834,#9296,#9297);
#9243=DIRECTION('axis',(0.,0.,1.));
#9244=DIRECTION('refdir',(1.,0.,0.));
#9245=DIRECTION('center_axis',(0.866025403784439,0.,-0.5));
#9246=DIRECTION('ref_axis',(0.5,0.,0.866025403784439));
#9247=DIRECTION('',(0.5,0.,0.866025403784439));
#9248=DIRECTION('',(0.,-1.,0.));
#9249=DIRECTION('',(0.5,0.,0.866025403784439));
#9250=DIRECTION('',(0.,-1.,0.));
#9251=DIRECTION('center_axis',(1.92296268638356E-16,0.,-1.));
#9252=DIRECTION('ref_axis',(1.,0.,1.92296268638356E-16));
#9253=DIRECTION('',(1.,0.,1.92296268638356E-16));
#9254=DIRECTION('',(0.,-1.,0.));
#9255=DIRECTION('',(1.,0.,1.92296268638356E-16));
#9256=DIRECTION('center_axis',(-0.866025403784439,0.,-0.5));
#9257=DIRECTION('ref_axis',(0.5,0.,-0.866025403784439));
#9258=DIRECTION('',(0.5,0.,-0.866025403784439));
#9259=DIRECTION('',(0.,-1.,0.));
#9260=DIRECTION('',(0.5,0.,-0.866025403784438));
#9261=DIRECTION('center_axis',(-0.866025403784439,0.,0.5));
#9262=DIRECTION('ref_axis',(-0.5,0.,-0.866025403784439));
#9263=DIRECTION('',(-0.5,0.,-0.866025403784439));
#9264=DIRECTION('',(0.,-1.,0.));
#9265=DIRECTION('',(-0.5,0.,-0.866025403784439));
#9266=DIRECTION('center_axis',(-1.92296268638356E-16,0.,1.));
#9267=DIRECTION('ref_axis',(-1.,0.,-1.92296268638356E-16));
#9268=DIRECTION('',(-1.,0.,-1.92296268638356E-16));
#9269=DIRECTION('',(0.,-1.,0.));
#9270=DIRECTION('',(-1.,0.,-1.92296268638356E-16));
#9271=DIRECTION('center_axis',(0.866025403784439,0.,0.5));
#9272=DIRECTION('ref_axis',(-0.5,0.,0.866025403784439));
#9273=DIRECTION('',(-0.5,0.,0.866025403784439));
#9274=DIRECTION('',(-0.5,0.,0.866025403784439));
#9275=DIRECTION('center_axis',(0.,-1.,0.));
#9276=DIRECTION('ref_axis',(0.,0.,-1.));
#9277=DIRECTION('center_axis',(0.,1.,0.));
#9278=DIRECTION('ref_axis',(0.,0.,1.));
#9279=DIRECTION('center_axis',(0.,-1.,0.));
#9280=DIRECTION('ref_axis',(1.,0.,0.));
#9281=DIRECTION('center_axis',(0.,-1.,0.));
#9282=DIRECTION('ref_axis',(1.,0.,0.));
#9283=DIRECTION('center_axis',(0.,-1.,0.));
#9284=DIRECTION('ref_axis',(1.,0.,0.));
#9285=DIRECTION('',(0.707106781186547,0.707106781186548,8.65956056235493E-17));
#9286=DIRECTION('center_axis',(0.,-1.,0.));
#9287=DIRECTION('ref_axis',(1.,0.,0.));
#9288=DIRECTION('center_axis',(0.,1.,0.));
#9289=DIRECTION('ref_axis',(1.,0.,0.));
#9290=DIRECTION('',(0.,1.,0.));
#9291=DIRECTION('center_axis',(0.,1.,0.));
#9292=DIRECTION('ref_axis',(1.,0.,0.));
#9293=DIRECTION('center_axis',(0.,-1.,0.));
#9294=DIRECTION('ref_axis',(1.,0.,0.));
#9295=DIRECTION('',(-0.707106781186547,0.707106781186548,-8.65956056235493E-17));
#9296=DIRECTION('center_axis',(0.,-1.,0.));
#9297=DIRECTION('ref_axis',(0.,0.,-1.));
#11781=CARTESIAN_POINT('',(0.,0.,0.));
#11782=CARTESIAN_POINT('Origin',(0.0721687836487032,0.,-0.125));
#11783=CARTESIAN_POINT('',(0.0721687836487032,0.,-0.125));
#11784=CARTESIAN_POINT('',(0.144337567297406,0.,0.));
#11785=CARTESIAN_POINT('',(0.117710979560879,0.,-0.0461186027918559));
#11786=CARTESIAN_POINT('',(0.0721687836487032,-0.25,-0.125));
#11787=CARTESIAN_POINT('',(0.0721687836487032,0.,-0.125));
#11788=CARTESIAN_POINT('',(0.144337567297406,-0.25,0.));
#11789=CARTESIAN_POINT('',(0.144337567297406,-0.25,0.));
#11790=CARTESIAN_POINT('',(0.144337567297406,0.,0.));
#11791=CARTESIAN_POINT('Origin',(-0.0721687836487032,0.,-0.125));
#11792=CARTESIAN_POINT('',(-0.0721687836487032,0.,-0.125));
#11793=CARTESIAN_POINT('',(0.0739156081756484,0.,-0.125));
#11794=CARTESIAN_POINT('',(-0.0721687836487032,-0.25,-0.125));
#11795=CARTESIAN_POINT('',(-0.0721687836487032,0.,-0.125));
#11796=CARTESIAN_POINT('',(0.0721687836487032,-0.25,-0.125));
#11797=CARTESIAN_POINT('Origin',(-0.144337567297406,0.,-4.16333634234434E-17));
#11798=CARTESIAN_POINT('',(-0.144337567297406,0.,-1.76762539787485E-17));
#11799=CARTESIAN_POINT('',(-0.0987953713852306,0.,-0.0788813972081442));
#11800=CARTESIAN_POINT('',(-0.144337567297406,-0.25,-2.77555756156289E-17));
#11801=CARTESIAN_POINT('',(-0.144337567297406,0.,-1.76762539787485E-17));
#11802=CARTESIAN_POINT('',(-0.0721687836487032,-0.25,-0.125));
#11803=CARTESIAN_POINT('Origin',(-0.0721687836487033,0.,0.125));
#11804=CARTESIAN_POINT('',(-0.0721687836487033,0.,0.125));
#11805=CARTESIAN_POINT('',(-0.0627109795608791,0.,0.141381397208144));
#11806=CARTESIAN_POINT('',(-0.0721687836487033,-0.25,0.125));
#11807=CARTESIAN_POINT('',(-0.0721687836487033,0.,0.125));
#11808=CARTESIAN_POINT('',(-0.144337567297406,-0.25,-1.76762539787485E-17));
#11809=CARTESIAN_POINT('Origin',(0.0721687836487032,0.,0.125));
#11810=CARTESIAN_POINT('',(0.0721687836487032,0.,0.125));
#11811=CARTESIAN_POINT('',(0.146084391824352,0.,0.125));
#11812=CARTESIAN_POINT('',(0.0721687836487032,-0.25,0.125));
#11813=CARTESIAN_POINT('',(0.0721687836487032,0.,0.125));
#11814=CARTESIAN_POINT('',(-0.0721687836487033,-0.25,0.125));
#11815=CARTESIAN_POINT('Origin',(0.144337567297406,0.,0.));
#11816=CARTESIAN_POINT('',(0.153795371385231,0.,-0.0163813972081441));
#11817=CARTESIAN_POINT('',(0.0721687836487032,-0.25,0.125));
#11818=CARTESIAN_POINT('Origin',(0.,-0.25,0.));
#11819=CARTESIAN_POINT('Origin',(0.22,0.,0.));
#11820=CARTESIAN_POINT('',(-0.22,-8.67361737988404E-18,-2.69422295812418E-17));
#11821=CARTESIAN_POINT('Origin',(0.,0.,0.));
#11822=CARTESIAN_POINT('Origin',(0.,-0.015,0.));
#11823=CARTESIAN_POINT('',(-0.24505,-0.02505,-3.00099698131059E-17));
#11824=CARTESIAN_POINT('Origin',(0.,-0.02505,0.));
#11825=CARTESIAN_POINT('',(-0.235,-0.015,-2.87791997799628E-17));
#11826=CARTESIAN_POINT('Origin',(0.,-0.3775,0.));
#11827=CARTESIAN_POINT('',(-0.24505,-0.72995,3.00099698131059E-17));
#11828=CARTESIAN_POINT('Origin',(0.,-0.72995,0.));
#11829=CARTESIAN_POINT('',(-0.24505,-0.3775,-3.00099698131059E-17));
#11830=CARTESIAN_POINT('Origin',(0.,-0.7625,0.));
#11831=CARTESIAN_POINT('',(-0.175,-0.8,-2.14313189850787E-17));
#11832=CARTESIAN_POINT('Origin',(0.,-0.8,0.));
#11833=CARTESIAN_POINT('',(-0.2125,-0.7625,-2.60237444818813E-17));
#11834=CARTESIAN_POINT('Origin',(0.,-0.8,0.));
#12722=UNCERTAINTY_MEASURE_WITH_UNIT(LENGTH_MEASURE(0.001),#12784,
'DISTANCE_ACCURACY_VALUE',
'Maximum model space distance between geometric entities at asserted c
onnectivities');
#12739=UNCERTAINTY_MEASURE_WITH_UNIT(LENGTH_MEASURE(0.001),#12784,
'DISTANCE_ACCURACY_VALUE',
'Maximum model space distance between geometric entities at asserted c
onnectivities');
#12766=(
GEOMETRIC_REPRESENTATION_CONTEXT(3)
GLOBAL_UNCERTAINTY_ASSIGNED_CONTEXT((#12722))
GLOBAL_UNIT_ASSIGNED_CONTEXT((#12784,#12786,#12787))
REPRESENTATION_CONTEXT('','3D')
);
#12783=(
GEOMETRIC_REPRESENTATION_CONTEXT(3)
GLOBAL_UNCERTAINTY_ASSIGNED_CONTEXT((#12739))
GLOBAL_UNIT_ASSIGNED_CONTEXT((#12784,#12786,#12787))
REPRESENTATION_CONTEXT('','3D')
);
#12784=(
LENGTH_UNIT()
NAMED_UNIT(*)
SI_UNIT(.CENTI.,.METRE.)
);
#12786=(
NAMED_UNIT(*)
PLANE_ANGLE_UNIT()
SI_UNIT($,.RADIAN.)
);
#12787=(
NAMED_UNIT(*)
SI_UNIT($,.STERADIAN.)
SOLID_ANGLE_UNIT()
);
#12814=SHAPE_DEFINITION_REPRESENTATION(#12883,#12957);
#12883=PRODUCT_DEFINITION_SHAPE('',$,#13001);
#12957=SHAPE_REPRESENTATION('',(#7520),#12766);
#12974=PRODUCT_DEFINITION_CONTEXT('part definition',#13105,'design');
#13001=PRODUCT_DEFINITION('Socket Set Screw - M5x8',
'Socket Set Screw - M5x8',#13044,#12974);
#13044=PRODUCT_DEFINITION_FORMATION('',$,#13133);
#13105=APPLICATION_CONTEXT(
'Core Data for Automotive Mechanical Design Process');
#13106=PRODUCT_CONTEXT('part definition',#13105,'mechanical');
#13133=PRODUCT('Socket Set Screw - M5x8','Socket Set Screw - M5x8',
'Socket Set Screw - M5x8',(#13106));
#13213=COLOUR_RGB('Black',0.12,0.14,0.17);
#13214=FILL_AREA_STYLE_COLOUR('',#13213);
#13215=FILL_AREA_STYLE('',(#13214));
#13216=SURFACE_STYLE_FILL_AREA(#13215);
#13217=SURFACE_SIDE_STYLE('',(#13216));
#13218=SURFACE_STYLE_USAGE(.BOTH.,#13217);
#13219=PRESENTATION_STYLE_ASSIGNMENT((#13218));
ENDSEC;
END-ISO-10303-21;
